ISO-10303-21;
HEADER;
/* Generated by software containing ST-Developer
 * from STEP Tools, Inc. (www.steptools.com) 
 */

FILE_DESCRIPTION(
/* description */ ('STEP AP214'),
/* implementation_level */ '2;1');

FILE_NAME(
/* name */ 'Socket Head Cap Screw M8 x 1.25 x 25.step',
/* time_stamp */ '2026-11-14T06:43:04-08:00',
/* author */ (''),
/* organization */ (''),
/* preprocessor_version */ 'ST-DEVELOPER v20.2',
/* originating_system */ 'Autodesk Translation Framework v15.17.0.0',
/* authorisation */ '');

FILE_SCHEMA (('AUTOMOTIVE_DESIGN { 1 0 10303 214 3 1 1 }'));
ENDSEC;

DATA;
#10=MECHANICAL_DESIGN_GEOMETRIC_PRESENTATION_REPRESENTATION('',(#208),#5658);
#114=CONICAL_SURFACE('',#3504,3.0475,1.04719755119659);
#115=CONICAL_SURFACE('',#3516,3.3095,0.785398163397565);
#116=CONICAL_SURFACE('',#3524,5.7,0.785398163397447);
#175=TOROIDAL_SURFACE('',#3511,4.40000000000003,0.4);
#186=SHAPE_REPRESENTATION_RELATIONSHIP('SRR','None',#5716,#197);
#197=ADVANCED_BREP_SHAPE_REPRESENTATION('',(#219),#5657);
#208=STYLED_ITEM('',(#5770),#219);
#219=MANIFOLD_SOLID_BREP('Body1',#3070);
#269=CYLINDRICAL_SURFACE('',#3519,4.00000000000003);
#270=CYLINDRICAL_SURFACE('',#3520,6.5);
#335=FACE_BOUND('',#751,.T.);
#336=FACE_BOUND('',#753,.T.);
#498=FACE_OUTER_BOUND('',#744,.T.);
#499=FACE_OUTER_BOUND('',#745,.T.);
#500=FACE_OUTER_BOUND('',#746,.T.);
#501=FACE_OUTER_BOUND('',#747,.T.);
#502=FACE_OUTER_BOUND('',#748,.T.);
#503=FACE_OUTER_BOUND('',#749,.T.);
#504=FACE_OUTER_BOUND('',#750,.T.);
#505=FACE_OUTER_BOUND('',#752,.T.);
#506=FACE_OUTER_BOUND('',#754,.T.);
#507=FACE_OUTER_BOUND('',#755,.T.);
#508=FACE_OUTER_BOUND('',#756,.T.);
#509=FACE_OUTER_BOUND('',#757,.T.);
#510=FACE_OUTER_BOUND('',#758,.T.);
#511=FACE_OUTER_BOUND('',#759,.T.);
#512=FACE_OUTER_BOUND('',#760,.T.);
#513=FACE_OUTER_BOUND('',#761,.T.);
#514=FACE_OUTER_BOUND('',#762,.T.);
#515=FACE_OUTER_BOUND('',#763,.T.);
#516=FACE_OUTER_BOUND('',#764,.T.);
#517=FACE_OUTER_BOUND('',#765,.T.);
#518=FACE_OUTER_BOUND('',#766,.T.);
#744=EDGE_LOOP('',(#2696,#2697,#2698,#2699,#2700,#2701,#2702,#2703));
#745=EDGE_LOOP('',(#2704,#2705,#2706,#2707,#2708));
#746=EDGE_LOOP('',(#2709,#2710,#2711,#2712));
#747=EDGE_LOOP('',(#2713,#2714,#2715,#2716,#2717));
#748=EDGE_LOOP('',(#2718,#2719,#2720,#2721,#2722));
#749=EDGE_LOOP('',(#2723,#2724,#2725,#2726,#2727));
#750=EDGE_LOOP('',(#2728));
#751=EDGE_LOOP('',(#2729,#2730,#2731,#2732,#2733,#2734));
#752=EDGE_LOOP('',(#2735));
#753=EDGE_LOOP('',(#2736));
#754=EDGE_LOOP('',(#2737));
#755=EDGE_LOOP('',(#2738,#2739,#2740,#2741,#2742));
#756=EDGE_LOOP('',(#2743,#2744,#2745,#2746,#2747));
#757=EDGE_LOOP('',(#2748,#2749,#2750,#2751,#2752));
#758=EDGE_LOOP('',(#2753,#2754,#2755,#2756,#2757));
#759=EDGE_LOOP('',(#2758,#2759,#2760,#2761,#2762));
#760=EDGE_LOOP('',(#2763,#2764,#2765,#2766,#2767));
#761=EDGE_LOOP('',(#2768,#2769,#2770));
#762=EDGE_LOOP('',(#2771,#2772,#2773));
#763=EDGE_LOOP('',(#2774,#2775,#2776));
#764=EDGE_LOOP('',(#2777,#2778,#2779));
#765=EDGE_LOOP('',(#2780,#2781,#2782));
#766=EDGE_LOOP('',(#2783,#2784,#2785));
#934=LINE('',#5524,#1130);
#935=LINE('',#5548,#1131);
#936=LINE('',#5551,#1132);
#937=LINE('',#5558,#1133);
#938=LINE('',#5562,#1134);
#939=LINE('',#5567,#1135);
#940=LINE('',#5569,#1136);
#941=LINE('',#5571,#1137);
#942=LINE('',#5573,#1138);
#943=LINE('',#5575,#1139);
#944=LINE('',#5576,#1140);
#945=LINE('',#5581,#1141);
#946=LINE('',#5582,#1142);
#947=LINE('',#5584,#1143);
#948=LINE('',#5585,#1144);
#949=LINE('',#5587,#1145);
#950=LINE('',#5589,#1146);
#951=LINE('',#5590,#1147);
#952=LINE('',#5592,#1148);
#953=LINE('',#5594,#1149);
#954=LINE('',#5595,#1150);
#955=LINE('',#5597,#1151);
#956=LINE('',#5599,#1152);
#957=LINE('',#5600,#1153);
#958=LINE('',#5602,#1154);
#959=LINE('',#5604,#1155);
#960=LINE('',#5605,#1156);
#961=LINE('',#5607,#1157);
#962=LINE('',#5608,#1158);
#1130=VECTOR('',#4350,3.0475);
#1131=VECTOR('',#4377,3.3095);
#1132=VECTOR('',#4382,4.00000000000003);
#1133=VECTOR('',#4389,6.5);
#1134=VECTOR('',#4394,5.7);
#1135=VECTOR('',#4399,1000.);
#1136=VECTOR('',#4400,1000.);
#1137=VECTOR('',#4401,1000.);
#1138=VECTOR('',#4402,1000.);
#1139=VECTOR('',#4403,1000.);
#1140=VECTOR('',#4404,1000.);
#1141=VECTOR('',#4411,1000.);
#1142=VECTOR('',#4412,1000.);
#1143=VECTOR('',#4413,1000.);
#1144=VECTOR('',#4414,1000.);
#1145=VECTOR('',#4417,1000.);
#1146=VECTOR('',#4418,1000.);
#1147=VECTOR('',#4419,1000.);
#1148=VECTOR('',#4422,1000.);
#1149=VECTOR('',#4423,1000.);
#1150=VECTOR('',#4424,1000.);
#1151=VECTOR('',#4427,1000.);
#1152=VECTOR('',#4428,1000.);
#1153=VECTOR('',#4429,1000.);
#1154=VECTOR('',#4432,1000.);
#1155=VECTOR('',#4433,1000.);
#1156=VECTOR('',#4434,1000.);
#1157=VECTOR('',#4437,1000.);
#1158=VECTOR('',#4438,1000.);
#1298=CIRCLE('',#3505,3.0475);
#1299=CIRCLE('',#3506,3.0475);
#1300=CIRCLE('',#3507,3.0475);
#1301=CIRCLE('',#3508,3.0475);
#1302=CIRCLE('',#3509,3.0475);
#1303=CIRCLE('',#3510,3.0475);
#1304=CIRCLE('',#3512,4.00000000000003);
#1305=CIRCLE('',#3513,4.00000000000003);
#1306=CIRCLE('',#3514,0.4);
#1307=CIRCLE('',#3515,4.40000000000003);
#1308=CIRCLE('',#3517,4.00000000000006);
#1309=CIRCLE('',#3518,3.3095);
#1310=CIRCLE('',#3521,6.5);
#1311=CIRCLE('',#3522,6.5);
#1312=CIRCLE('',#3523,6.5);
#1313=CIRCLE('',#3525,5.7);
#1543=VERTEX_POINT('',#5522);
#1544=VERTEX_POINT('',#5523);
#1545=VERTEX_POINT('',#5525);
#1546=VERTEX_POINT('',#5527);
#1547=VERTEX_POINT('',#5529);
#1548=VERTEX_POINT('',#5531);
#1549=VERTEX_POINT('',#5533);
#1550=VERTEX_POINT('',#5537);
#1551=VERTEX_POINT('',#5538);
#1552=VERTEX_POINT('',#5541);
#1553=VERTEX_POINT('',#5545);
#1554=VERTEX_POINT('',#5547);
#1555=VERTEX_POINT('',#5553);
#1556=VERTEX_POINT('',#5554);
#1557=VERTEX_POINT('',#5557);
#1558=VERTEX_POINT('',#5561);
#1559=VERTEX_POINT('',#5565);
#1560=VERTEX_POINT('',#5566);
#1561=VERTEX_POINT('',#5568);
#1562=VERTEX_POINT('',#5570);
#1563=VERTEX_POINT('',#5572);
#1564=VERTEX_POINT('',#5574);
#1565=VERTEX_POINT('',#5580);
#1566=VERTEX_POINT('',#5583);
#1567=VERTEX_POINT('',#5588);
#1568=VERTEX_POINT('',#5593);
#1569=VERTEX_POINT('',#5598);
#1570=VERTEX_POINT('',#5603);
#1931=EDGE_CURVE('',#1543,#1544,#934,.T.);
#1932=EDGE_CURVE('',#1544,#1545,#1298,.T.);
#1933=EDGE_CURVE('',#1545,#1546,#1299,.T.);
#1934=EDGE_CURVE('',#1546,#1547,#1300,.T.);
#1935=EDGE_CURVE('',#1547,#1548,#1301,.T.);
#1936=EDGE_CURVE('',#1548,#1549,#1302,.T.);
#1937=EDGE_CURVE('',#1549,#1544,#1303,.T.);
#1938=EDGE_CURVE('',#1550,#1551,#1304,.T.);
#1939=EDGE_CURVE('',#1551,#1550,#1305,.T.);
#1940=EDGE_CURVE('',#1551,#1552,#1306,.T.);
#1941=EDGE_CURVE('',#1552,#1552,#1307,.T.);
#1942=EDGE_CURVE('',#1553,#1553,#1308,.T.);
#1943=EDGE_CURVE('',#1553,#1554,#935,.T.);
#1944=EDGE_CURVE('',#1554,#1554,#1309,.T.);
#1945=EDGE_CURVE('',#1550,#1553,#936,.T.);
#1946=EDGE_CURVE('',#1555,#1556,#1310,.T.);
#1947=EDGE_CURVE('',#1556,#1555,#1311,.T.);
#1948=EDGE_CURVE('',#1556,#1557,#937,.T.);
#1949=EDGE_CURVE('',#1557,#1557,#1312,.T.);
#1950=EDGE_CURVE('',#1555,#1558,#938,.T.);
#1951=EDGE_CURVE('',#1558,#1558,#1313,.T.);
#1952=EDGE_CURVE('',#1559,#1560,#939,.T.);
#1953=EDGE_CURVE('',#1561,#1560,#940,.T.);
#1954=EDGE_CURVE('',#1561,#1562,#941,.T.);
#1955=EDGE_CURVE('',#1562,#1563,#942,.T.);
#1956=EDGE_CURVE('',#1564,#1563,#943,.T.);
#1957=EDGE_CURVE('',#1559,#1564,#944,.T.);
#1958=EDGE_CURVE('',#1565,#1559,#945,.T.);
#1959=EDGE_CURVE('',#1565,#1548,#946,.T.);
#1960=EDGE_CURVE('',#1548,#1566,#947,.T.);
#1961=EDGE_CURVE('',#1566,#1560,#948,.T.);
#1962=EDGE_CURVE('',#1547,#1566,#949,.T.);
#1963=EDGE_CURVE('',#1567,#1547,#950,.T.);
#1964=EDGE_CURVE('',#1567,#1561,#951,.T.);
#1965=EDGE_CURVE('',#1567,#1546,#952,.T.);
#1966=EDGE_CURVE('',#1546,#1568,#953,.T.);
#1967=EDGE_CURVE('',#1568,#1562,#954,.T.);
#1968=EDGE_CURVE('',#1568,#1545,#955,.T.);
#1969=EDGE_CURVE('',#1545,#1569,#956,.T.);
#1970=EDGE_CURVE('',#1569,#1563,#957,.T.);
#1971=EDGE_CURVE('',#1544,#1569,#958,.T.);
#1972=EDGE_CURVE('',#1570,#1544,#959,.T.);
#1973=EDGE_CURVE('',#1570,#1564,#960,.T.);
#1974=EDGE_CURVE('',#1549,#1570,#961,.T.);
#1975=EDGE_CURVE('',#1565,#1549,#962,.T.);
#2696=ORIENTED_EDGE('',*,*,#1931,.T.);
#2697=ORIENTED_EDGE('',*,*,#1932,.T.);
#2698=ORIENTED_EDGE('',*,*,#1933,.T.);
#2699=ORIENTED_EDGE('',*,*,#1934,.T.);
#2700=ORIENTED_EDGE('',*,*,#1935,.T.);
#2701=ORIENTED_EDGE('',*,*,#1936,.T.);
#2702=ORIENTED_EDGE('',*,*,#1937,.T.);
#2703=ORIENTED_EDGE('',*,*,#1931,.F.);
#2704=ORIENTED_EDGE('',*,*,#1938,.F.);
#2705=ORIENTED_EDGE('',*,*,#1939,.F.);
#2706=ORIENTED_EDGE('',*,*,#1940,.T.);
#2707=ORIENTED_EDGE('',*,*,#1941,.F.);
#2708=ORIENTED_EDGE('',*,*,#1940,.F.);
#2709=ORIENTED_EDGE('',*,*,#1942,.F.);
#2710=ORIENTED_EDGE('',*,*,#1943,.T.);
#2711=ORIENTED_EDGE('',*,*,#1944,.T.);
#2712=ORIENTED_EDGE('',*,*,#1943,.F.);
#2713=ORIENTED_EDGE('',*,*,#1938,.T.);
#2714=ORIENTED_EDGE('',*,*,#1939,.T.);
#2715=ORIENTED_EDGE('',*,*,#1945,.T.);
#2716=ORIENTED_EDGE('',*,*,#1942,.T.);
#2717=ORIENTED_EDGE('',*,*,#1945,.F.);
#2718=ORIENTED_EDGE('',*,*,#1946,.F.);
#2719=ORIENTED_EDGE('',*,*,#1947,.F.);
#2720=ORIENTED_EDGE('',*,*,#1948,.T.);
#2721=ORIENTED_EDGE('',*,*,#1949,.T.);
#2722=ORIENTED_EDGE('',*,*,#1948,.F.);
#2723=ORIENTED_EDGE('',*,*,#1946,.T.);
#2724=ORIENTED_EDGE('',*,*,#1947,.T.);
#2725=ORIENTED_EDGE('',*,*,#1950,.T.);
#2726=ORIENTED_EDGE('',*,*,#1951,.F.);
#2727=ORIENTED_EDGE('',*,*,#1950,.F.);
#2728=ORIENTED_EDGE('',*,*,#1951,.T.);
#2729=ORIENTED_EDGE('',*,*,#1952,.T.);
#2730=ORIENTED_EDGE('',*,*,#1953,.F.);
#2731=ORIENTED_EDGE('',*,*,#1954,.T.);
#2732=ORIENTED_EDGE('',*,*,#1955,.T.);
#2733=ORIENTED_EDGE('',*,*,#1956,.F.);
#2734=ORIENTED_EDGE('',*,*,#1957,.F.);
#2735=ORIENTED_EDGE('',*,*,#1949,.F.);
#2736=ORIENTED_EDGE('',*,*,#1941,.T.);
#2737=ORIENTED_EDGE('',*,*,#1944,.F.);
#2738=ORIENTED_EDGE('',*,*,#1952,.F.);
#2739=ORIENTED_EDGE('',*,*,#1958,.F.);
#2740=ORIENTED_EDGE('',*,*,#1959,.T.);
#2741=ORIENTED_EDGE('',*,*,#1960,.T.);
#2742=ORIENTED_EDGE('',*,*,#1961,.T.);
#2743=ORIENTED_EDGE('',*,*,#1953,.T.);
#2744=ORIENTED_EDGE('',*,*,#1961,.F.);
#2745=ORIENTED_EDGE('',*,*,#1962,.F.);
#2746=ORIENTED_EDGE('',*,*,#1963,.F.);
#2747=ORIENTED_EDGE('',*,*,#1964,.T.);
#2748=ORIENTED_EDGE('',*,*,#1954,.F.);
#2749=ORIENTED_EDGE('',*,*,#1964,.F.);
#2750=ORIENTED_EDGE('',*,*,#1965,.T.);
#2751=ORIENTED_EDGE('',*,*,#1966,.T.);
#2752=ORIENTED_EDGE('',*,*,#1967,.T.);
#2753=ORIENTED_EDGE('',*,*,#1955,.F.);
#2754=ORIENTED_EDGE('',*,*,#1967,.F.);
#2755=ORIENTED_EDGE('',*,*,#1968,.T.);
#2756=ORIENTED_EDGE('',*,*,#1969,.T.);
#2757=ORIENTED_EDGE('',*,*,#1970,.T.);
#2758=ORIENTED_EDGE('',*,*,#1956,.T.);
#2759=ORIENTED_EDGE('',*,*,#1970,.F.);
#2760=ORIENTED_EDGE('',*,*,#1971,.F.);
#2761=ORIENTED_EDGE('',*,*,#1972,.F.);
#2762=ORIENTED_EDGE('',*,*,#1973,.T.);
#2763=ORIENTED_EDGE('',*,*,#1957,.T.);
#2764=ORIENTED_EDGE('',*,*,#1973,.F.);
#2765=ORIENTED_EDGE('',*,*,#1974,.F.);
#2766=ORIENTED_EDGE('',*,*,#1975,.F.);
#2767=ORIENTED_EDGE('',*,*,#1958,.T.);
#2768=ORIENTED_EDGE('',*,*,#1934,.F.);
#2769=ORIENTED_EDGE('',*,*,#1965,.F.);
#2770=ORIENTED_EDGE('',*,*,#1963,.T.);
#2771=ORIENTED_EDGE('',*,*,#1933,.F.);
#2772=ORIENTED_EDGE('',*,*,#1968,.F.);
#2773=ORIENTED_EDGE('',*,*,#1966,.F.);
#2774=ORIENTED_EDGE('',*,*,#1932,.F.);
#2775=ORIENTED_EDGE('',*,*,#1971,.T.);
#2776=ORIENTED_EDGE('',*,*,#1969,.F.);
#2777=ORIENTED_EDGE('',*,*,#1937,.F.);
#2778=ORIENTED_EDGE('',*,*,#1974,.T.);
#2779=ORIENTED_EDGE('',*,*,#1972,.T.);
#2780=ORIENTED_EDGE('',*,*,#1936,.F.);
#2781=ORIENTED_EDGE('',*,*,#1959,.F.);
#2782=ORIENTED_EDGE('',*,*,#1975,.T.);
#2783=ORIENTED_EDGE('',*,*,#1935,.F.);
#2784=ORIENTED_EDGE('',*,*,#1962,.T.);
#2785=ORIENTED_EDGE('',*,*,#1960,.F.);
#2863=PLANE('',#3526);
#2864=PLANE('',#3527);
#2865=PLANE('',#3528);
#2866=PLANE('',#3529);
#2867=PLANE('',#3530);
#2868=PLANE('',#3531);
#2869=PLANE('',#3532);
#2870=PLANE('',#3533);
#2871=PLANE('',#3534);
#2872=PLANE('',#3535);
#2873=PLANE('',#3536);
#2874=PLANE('',#3537);
#2875=PLANE('',#3538);
#2876=PLANE('',#3539);
#2877=PLANE('',#3540);
#3039=ADVANCED_FACE('',(#498),#114,.F.);
#3040=ADVANCED_FACE('',(#499),#175,.F.);
#3041=ADVANCED_FACE('',(#500),#115,.T.);
#3042=ADVANCED_FACE('',(#501),#269,.T.);
#3043=ADVANCED_FACE('',(#502),#270,.T.);
#3044=ADVANCED_FACE('',(#503),#116,.T.);
#3045=ADVANCED_FACE('',(#504,#335),#2863,.T.);
#3046=ADVANCED_FACE('',(#505,#336),#2864,.T.);
#3047=ADVANCED_FACE('',(#506),#2865,.T.);
#3048=ADVANCED_FACE('',(#507),#2866,.T.);
#3049=ADVANCED_FACE('',(#508),#2867,.F.);
#3050=ADVANCED_FACE('',(#509),#2868,.T.);
#3051=ADVANCED_FACE('',(#510),#2869,.T.);
#3052=ADVANCED_FACE('',(#511),#2870,.F.);
#3053=ADVANCED_FACE('',(#512),#2871,.F.);
#3054=ADVANCED_FACE('',(#513),#2872,.T.);
#3055=ADVANCED_FACE('',(#514),#2873,.T.);
#3056=ADVANCED_FACE('',(#515),#2874,.T.);
#3057=ADVANCED_FACE('',(#516),#2875,.T.);
#3058=ADVANCED_FACE('',(#517),#2876,.T.);
#3059=ADVANCED_FACE('',(#518),#2877,.T.);
#3070=CLOSED_SHELL('',(#3039,#3040,#3041,#3042,#3043,#3044,#3045,#3046,
#3047,#3048,#3049,#3050,#3051,#3052,#3053,#3054,#3055,#3056,#3057,#3058,
#3059));
#3503=AXIS2_PLACEMENT_3D('',#5520,#4346,#4347);
#3504=AXIS2_PLACEMENT_3D('',#5521,#4348,#4349);
#3505=AXIS2_PLACEMENT_3D('',#5526,#4351,#4352);
#3506=AXIS2_PLACEMENT_3D('',#5528,#4353,#4354);
#3507=AXIS2_PLACEMENT_3D('',#5530,#4355,#4356);
#3508=AXIS2_PLACEMENT_3D('',#5532,#4357,#4358);
#3509=AXIS2_PLACEMENT_3D('',#5534,#4359,#4360);
#3510=AXIS2_PLACEMENT_3D('',#5535,#4361,#4362);
#3511=AXIS2_PLACEMENT_3D('',#5536,#4363,#4364);
#3512=AXIS2_PLACEMENT_3D('',#5539,#4365,#4366);
#3513=AXIS2_PLACEMENT_3D('',#5540,#4367,#4368);
#3514=AXIS2_PLACEMENT_3D('',#5542,#4369,#4370);
#3515=AXIS2_PLACEMENT_3D('',#5543,#4371,#4372);
#3516=AXIS2_PLACEMENT_3D('',#5544,#4373,#4374);
#3517=AXIS2_PLACEMENT_3D('',#5546,#4375,#4376);
#3518=AXIS2_PLACEMENT_3D('',#5549,#4378,#4379);
#3519=AXIS2_PLACEMENT_3D('',#5550,#4380,#4381);
#3520=AXIS2_PLACEMENT_3D('',#5552,#4383,#4384);
#3521=AXIS2_PLACEMENT_3D('',#5555,#4385,#4386);
#3522=AXIS2_PLACEMENT_3D('',#5556,#4387,#4388);
#3523=AXIS2_PLACEMENT_3D('',#5559,#4390,#4391);
#3524=AXIS2_PLACEMENT_3D('',#5560,#4392,#4393);
#3525=AXIS2_PLACEMENT_3D('',#5563,#4395,#4396);
#3526=AXIS2_PLACEMENT_3D('',#5564,#4397,#4398);
#3527=AXIS2_PLACEMENT_3D('',#5577,#4405,#4406);
#3528=AXIS2_PLACEMENT_3D('',#5578,#4407,#4408);
#3529=AXIS2_PLACEMENT_3D('',#5579,#4409,#4410);
#3530=AXIS2_PLACEMENT_3D('',#5586,#4415,#4416);
#3531=AXIS2_PLACEMENT_3D('',#5591,#4420,#4421);
#3532=AXIS2_PLACEMENT_3D('',#5596,#4425,#4426);
#3533=AXIS2_PLACEMENT_3D('',#5601,#4430,#4431);
#3534=AXIS2_PLACEMENT_3D('',#5606,#4435,#4436);
#3535=AXIS2_PLACEMENT_3D('',#5609,#4439,#4440);
#3536=AXIS2_PLACEMENT_3D('',#5610,#4441,#4442);
#3537=AXIS2_PLACEMENT_3D('',#5611,#4443,#4444);
#3538=AXIS2_PLACEMENT_3D('',#5612,#4445,#4446);
#3539=AXIS2_PLACEMENT_3D('',#5613,#4447,#4448);
#3540=AXIS2_PLACEMENT_3D('',#5614,#4449,#4450);
#4346=DIRECTION('axis',(0.,0.,1.));
#4347=DIRECTION('refdir',(1.,0.,0.));
#4348=DIRECTION('center_axis',(-1.,0.,0.));
#4349=DIRECTION('ref_axis',(0.,0.,1.));
#4350=DIRECTION('',(-0.500000000000005,-1.0605752387249E-16,-0.866025403784436));
#4351=DIRECTION('center_axis',(-1.,0.,0.));
#4352=DIRECTION('ref_axis',(0.,0.,1.));
#4353=DIRECTION('center_axis',(-1.,0.,0.));
#4354=DIRECTION('ref_axis',(0.,0.,1.));
#4355=DIRECTION('center_axis',(-1.,0.,0.));
#4356=DIRECTION('ref_axis',(0.,0.,1.));
#4357=DIRECTION('center_axis',(-1.,0.,0.));
#4358=DIRECTION('ref_axis',(0.,0.,1.));
#4359=DIRECTION('center_axis',(-1.,0.,0.));
#4360=DIRECTION('ref_axis',(0.,0.,1.));
#4361=DIRECTION('center_axis',(-1.,0.,0.));
#4362=DIRECTION('ref_axis',(0.,0.,1.));
#4363=DIRECTION('center_axis',(1.,0.,0.));
#4364=DIRECTION('ref_axis',(0.,0.,-1.));
#4365=DIRECTION('center_axis',(1.,0.,0.));
#4366=DIRECTION('ref_axis',(0.,0.,-1.));
#4367=DIRECTION('center_axis',(1.,0.,0.));
#4368=DIRECTION('ref_axis',(0.,0.,-1.));
#4369=DIRECTION('center_axis',(0.,1.,1.22464679914735E-16));
#4370=DIRECTION('ref_axis',(0.,-1.22464679914735E-16,1.));
#4371=DIRECTION('center_axis',(-1.,0.,0.));
#4372=DIRECTION('ref_axis',(0.,0.,-1.));
#4373=DIRECTION('center_axis',(-1.,0.,0.));
#4374=DIRECTION('ref_axis',(0.,0.,1.));
#4375=DIRECTION('center_axis',(-1.,0.,0.));
#4376=DIRECTION('ref_axis',(0.,0.,1.));
#4377=DIRECTION('',(0.707106781186465,8.65956056235594E-17,0.70710678118663));
#4378=DIRECTION('center_axis',(-1.,0.,0.));
#4379=DIRECTION('ref_axis',(0.,0.,1.));
#4380=DIRECTION('center_axis',(-1.,0.,0.));
#4381=DIRECTION('ref_axis',(0.,0.,1.));
#4382=DIRECTION('',(1.,0.,0.));
#4383=DIRECTION('center_axis',(-1.,0.,0.));
#4384=DIRECTION('ref_axis',(0.,0.,1.));
#4385=DIRECTION('center_axis',(-1.,0.,0.));
#4386=DIRECTION('ref_axis',(0.,0.,1.));
#4387=DIRECTION('center_axis',(-1.,0.,0.));
#4388=DIRECTION('ref_axis',(0.,0.,1.));
#4389=DIRECTION('',(1.,0.,0.));
#4390=DIRECTION('center_axis',(-1.,0.,0.));
#4391=DIRECTION('ref_axis',(0.,0.,1.));
#4392=DIRECTION('center_axis',(1.,0.,0.));
#4393=DIRECTION('ref_axis',(0.,0.,-1.));
#4394=DIRECTION('',(-0.707106781186548,8.65956056235492E-17,-0.707106781186547));
#4395=DIRECTION('center_axis',(-1.,0.,0.));
#4396=DIRECTION('ref_axis',(0.,0.,1.));
#4397=DIRECTION('center_axis',(-1.,0.,0.));
#4398=DIRECTION('ref_axis',(0.,0.,1.));
#4399=DIRECTION('',(0.,-0.499999999999998,0.866025403784439));
#4400=DIRECTION('',(0.,1.,-8.62690909857269E-16));
#4401=DIRECTION('',(0.,-0.500000000000001,-0.866025403784438));
#4402=DIRECTION('',(0.,0.499999999999999,-0.866025403784439));
#4403=DIRECTION('',(0.,-1.,1.47889870261246E-15));
#4404=DIRECTION('',(0.,-0.500000000000001,-0.866025403784438));
#4405=DIRECTION('center_axis',(1.,0.,0.));
#4406=DIRECTION('ref_axis',(0.,0.,-1.));
#4407=DIRECTION('center_axis',(1.,0.,0.));
#4408=DIRECTION('ref_axis',(0.,0.,-1.));
#4409=DIRECTION('center_axis',(0.,-0.86602540378444,-0.499999999999998));
#4410=DIRECTION('ref_axis',(0.,0.499999999999998,-0.86602540378444));
#4411=DIRECTION('',(-1.,0.,0.));
#4412=DIRECTION('',(0.,-0.499999999999998,0.866025403784439));
#4413=DIRECTION('',(0.,-0.499999999999998,0.866025403784439));
#4414=DIRECTION('',(-1.,0.,0.));
#4415=DIRECTION('center_axis',(0.,8.62690909857269E-16,1.));
#4416=DIRECTION('ref_axis',(0.,-1.,8.62690909857269E-16));
#4417=DIRECTION('',(0.,1.,-8.62690909857269E-16));
#4418=DIRECTION('',(0.,1.,-8.62690909857269E-16));
#4419=DIRECTION('',(-1.,0.,0.));
#4420=DIRECTION('center_axis',(0.,0.866025403784438,-0.500000000000001));
#4421=DIRECTION('ref_axis',(0.,0.500000000000001,0.866025403784438));
#4422=DIRECTION('',(0.,-0.500000000000001,-0.866025403784438));
#4423=DIRECTION('',(0.,-0.500000000000001,-0.866025403784438));
#4424=DIRECTION('',(-1.,0.,0.));
#4425=DIRECTION('center_axis',(0.,0.866025403784439,0.499999999999999));
#4426=DIRECTION('ref_axis',(0.,-0.499999999999999,0.866025403784439));
#4427=DIRECTION('',(0.,0.499999999999999,-0.866025403784439));
#4428=DIRECTION('',(0.,0.499999999999999,-0.866025403784439));
#4429=DIRECTION('',(-1.,0.,0.));
#4430=DIRECTION('center_axis',(0.,-1.47889870261246E-15,-1.));
#4431=DIRECTION('ref_axis',(0.,1.,-1.47889870261246E-15));
#4432=DIRECTION('',(0.,-1.,1.47889870261246E-15));
#4433=DIRECTION('',(0.,-1.,1.47889870261246E-15));
#4434=DIRECTION('',(-1.,0.,0.));
#4435=DIRECTION('center_axis',(0.,0.866025403784438,-0.500000000000001));
#4436=DIRECTION('ref_axis',(0.,0.500000000000001,0.866025403784438));
#4437=DIRECTION('',(0.,-0.500000000000001,-0.866025403784438));
#4438=DIRECTION('',(0.,-0.500000000000001,-0.866025403784438));
#4439=DIRECTION('center_axis',(-1.,0.,0.));
#4440=DIRECTION('ref_axis',(0.,0.,1.));
#4441=DIRECTION('center_axis',(-1.,0.,0.));
#4442=DIRECTION('ref_axis',(0.,0.,1.));
#4443=DIRECTION('center_axis',(-1.,0.,0.));
#4444=DIRECTION('ref_axis',(0.,0.,1.));
#4445=DIRECTION('center_axis',(-1.,0.,0.));
#4446=DIRECTION('ref_axis',(0.,0.,1.));
#4447=DIRECTION('center_axis',(-1.,0.,0.));
#4448=DIRECTION('ref_axis',(0.,0.,1.));
#4449=DIRECTION('center_axis',(-1.,0.,0.));
#4450=DIRECTION('ref_axis',(0.,0.,1.));
#5520=CARTESIAN_POINT('',(0.,0.,0.));
#5521=CARTESIAN_POINT('Origin',(4.00000000000001,0.,0.));
#5522=CARTESIAN_POINT('',(5.75947494535541,0.,0.));
#5523=CARTESIAN_POINT('',(4.,-4.50694379621148E-15,-3.0475));
#5524=CARTESIAN_POINT('',(4.00000000000001,-3.73211112040156E-16,-3.0475));
#5525=CARTESIAN_POINT('',(4.,-2.63921241803308,-1.52375));
#5526=CARTESIAN_POINT('Origin',(4.00000000000001,0.,0.));
#5527=CARTESIAN_POINT('',(4.,-2.63921241803307,1.52375));
#5528=CARTESIAN_POINT('Origin',(4.00000000000001,0.,0.));
#5529=CARTESIAN_POINT('',(4.,2.62905054779003E-15,3.0475));
#5530=CARTESIAN_POINT('Origin',(4.00000000000001,0.,0.));
#5531=CARTESIAN_POINT('',(4.00000000000001,2.63921241803308,1.52375));
#5532=CARTESIAN_POINT('Origin',(4.00000000000001,0.,0.));
#5533=CARTESIAN_POINT('',(4.,2.63921241803308,-1.52375));
#5534=CARTESIAN_POINT('Origin',(4.00000000000001,0.,0.));
#5535=CARTESIAN_POINT('Origin',(4.00000000000001,0.,0.));
#5536=CARTESIAN_POINT('Origin',(8.4,0.,0.));
#5537=CARTESIAN_POINT('',(8.4,4.89858719658945E-16,-4.00000000000003));
#5538=CARTESIAN_POINT('',(8.4,-4.89858719658945E-16,4.00000000000003));
#5539=CARTESIAN_POINT('Origin',(8.4,0.,0.));
#5540=CARTESIAN_POINT('Origin',(8.4,0.,0.));
#5541=CARTESIAN_POINT('',(8.,-5.38844591624839E-16,4.40000000000003));
#5542=CARTESIAN_POINT('Origin',(8.4,-5.38844591624839E-16,4.40000000000003));
#5543=CARTESIAN_POINT('Origin',(8.,0.,0.));
#5544=CARTESIAN_POINT('Origin',(33.,0.,0.));
#5545=CARTESIAN_POINT('',(32.3095000000001,-4.89858719658949E-16,-4.00000000000006));
#5546=CARTESIAN_POINT('Origin',(32.3095000000001,0.,0.));
#5547=CARTESIAN_POINT('',(33.,-4.05296858177817E-16,-3.3095));
#5548=CARTESIAN_POINT('',(33.,-4.05296858177817E-16,-3.3095));
#5549=CARTESIAN_POINT('Origin',(33.,0.,0.));
#5550=CARTESIAN_POINT('Origin',(-31.75,0.,0.));
#5551=CARTESIAN_POINT('',(-31.75,-4.89858719658945E-16,-4.00000000000003));
#5552=CARTESIAN_POINT('Origin',(-31.75,0.,0.));
#5553=CARTESIAN_POINT('',(0.800000000000002,7.9602041944578E-16,6.5));
#5554=CARTESIAN_POINT('',(0.800000000000001,-7.9602041944578E-16,-6.5));
#5555=CARTESIAN_POINT('Origin',(0.800000000000002,0.,0.));
#5556=CARTESIAN_POINT('Origin',(0.800000000000002,0.,0.));
#5557=CARTESIAN_POINT('',(8.00000000000001,-7.9602041944578E-16,-6.5));
#5558=CARTESIAN_POINT('',(-31.75,-7.9602041944578E-16,-6.5));
#5559=CARTESIAN_POINT('Origin',(8.00000000000001,0.,0.));
#5560=CARTESIAN_POINT('Origin',(0.,0.,0.));
#5561=CARTESIAN_POINT('',(-2.19298459084284E-16,-6.98048675513992E-16,5.7));
#5562=CARTESIAN_POINT('',(0.,-6.98048675513992E-16,5.7));
#5563=CARTESIAN_POINT('Origin',(0.,0.,0.));
#5564=CARTESIAN_POINT('Origin',(-3.19315087200652E-17,0.,0.));
#5565=CARTESIAN_POINT('',(0.,3.51894989071077,-3.46944695195361E-15));
#5566=CARTESIAN_POINT('',(0.,1.75947494535539,3.0475));
#5567=CARTESIAN_POINT('',(0.,3.51894989071077,-3.46944695195361E-15));
#5568=CARTESIAN_POINT('',(0.,-1.75947494535538,3.0475));
#5569=CARTESIAN_POINT('',(0.,-1.75947494535538,3.0475));
#5570=CARTESIAN_POINT('',(0.,-3.51894989071077,5.20417042793042E-15));
#5571=CARTESIAN_POINT('',(0.,-1.75947494535538,3.0475));
#5572=CARTESIAN_POINT('',(0.,-1.75947494535539,-3.0475));
#5573=CARTESIAN_POINT('',(0.,-3.51894989071077,5.20417042793042E-15));
#5574=CARTESIAN_POINT('',(0.,1.75947494535538,-3.0475));
#5575=CARTESIAN_POINT('',(0.,1.75947494535538,-3.0475));
#5576=CARTESIAN_POINT('',(0.,3.51894989071077,-3.46944695195361E-15));
#5577=CARTESIAN_POINT('Origin',(8.,6.5,0.));
#5578=CARTESIAN_POINT('Origin',(33.,3.3095,0.));
#5579=CARTESIAN_POINT('Origin',(4.,3.51894989071077,-3.46944695195361E-15));
#5580=CARTESIAN_POINT('',(4.,3.51894989071077,-3.46944695195361E-15));
#5581=CARTESIAN_POINT('',(4.,3.51894989071077,-3.46944695195361E-15));
#5582=CARTESIAN_POINT('',(4.,3.51894989071077,-3.46944695195361E-15));
#5583=CARTESIAN_POINT('',(4.,1.75947494535539,3.0475));
#5584=CARTESIAN_POINT('',(4.,3.51894989071077,-3.46944695195361E-15));
#5585=CARTESIAN_POINT('',(4.,1.75947494535539,3.0475));
#5586=CARTESIAN_POINT('Origin',(4.,-1.75947494535538,3.0475));
#5587=CARTESIAN_POINT('',(4.,-1.75947494535538,3.0475));
#5588=CARTESIAN_POINT('',(4.,-1.75947494535538,3.0475));
#5589=CARTESIAN_POINT('',(4.,-1.75947494535538,3.0475));
#5590=CARTESIAN_POINT('',(4.,-1.75947494535538,3.0475));
#5591=CARTESIAN_POINT('Origin',(4.,-1.75947494535538,3.0475));
#5592=CARTESIAN_POINT('',(4.,-1.75947494535538,3.0475));
#5593=CARTESIAN_POINT('',(4.,-3.51894989071077,5.20417042793042E-15));
#5594=CARTESIAN_POINT('',(4.,-1.75947494535538,3.0475));
#5595=CARTESIAN_POINT('',(4.,-3.51894989071077,5.20417042793042E-15));
#5596=CARTESIAN_POINT('Origin',(4.,-3.51894989071077,5.20417042793042E-15));
#5597=CARTESIAN_POINT('',(4.,-3.51894989071077,5.20417042793042E-15));
#5598=CARTESIAN_POINT('',(4.,-1.75947494535539,-3.0475));
#5599=CARTESIAN_POINT('',(4.,-3.51894989071077,5.20417042793042E-15));
#5600=CARTESIAN_POINT('',(4.,-1.75947494535539,-3.0475));
#5601=CARTESIAN_POINT('Origin',(4.,1.75947494535538,-3.0475));
#5602=CARTESIAN_POINT('',(4.,1.75947494535538,-3.0475));
#5603=CARTESIAN_POINT('',(4.,1.75947494535538,-3.0475));
#5604=CARTESIAN_POINT('',(4.,1.75947494535538,-3.0475));
#5605=CARTESIAN_POINT('',(4.,1.75947494535538,-3.0475));
#5606=CARTESIAN_POINT('Origin',(4.,3.51894989071077,-3.46944695195361E-15));
#5607=CARTESIAN_POINT('',(4.,3.51894989071077,-3.46944695195361E-15));
#5608=CARTESIAN_POINT('',(4.,3.51894989071077,-3.46944695195361E-15));
#5609=CARTESIAN_POINT('Origin',(4.,1.75947494535539,3.0475));
#5610=CARTESIAN_POINT('Origin',(4.,1.75947494535539,3.0475));
#5611=CARTESIAN_POINT('Origin',(4.,1.75947494535539,3.0475));
#5612=CARTESIAN_POINT('Origin',(4.,1.75947494535539,3.0475));
#5613=CARTESIAN_POINT('Origin',(4.,1.75947494535539,3.0475));
#5614=CARTESIAN_POINT('Origin',(4.,1.75947494535539,3.0475));
#5644=UNCERTAINTY_MEASURE_WITH_UNIT(LENGTH_MEASURE(0.01),#5659,
'DISTANCE_ACCURACY_VALUE',
'Maximum model space distance between geometric entities at asserted c
onnectivities');
#5645=UNCERTAINTY_MEASURE_WITH_UNIT(LENGTH_MEASURE(0.01),#5659,
'DISTANCE_ACCURACY_VALUE',
'Maximum model space distance between geometric entities at asserted c
onnectivities');
#5657=(
GEOMETRIC_REPRESENTATION_CONTEXT(3)
GLOBAL_UNCERTAINTY_ASSIGNED_CONTEXT((#5644))
GLOBAL_UNIT_ASSIGNED_CONTEXT((#5659,#5661,#5662))
REPRESENTATION_CONTEXT('','3D')
);
#5658=(
GEOMETRIC_REPRESENTATION_CONTEXT(3)
GLOBAL_UNCERTAINTY_ASSIGNED_CONTEXT((#5645))
GLOBAL_UNIT_ASSIGNED_CONTEXT((#5659,#5661,#5662))
REPRESENTATION_CONTEXT('','3D')
);
#5659=(
LENGTH_UNIT()
NAMED_UNIT(*)
SI_UNIT(.MILLI.,.METRE.)
);
#5661=(
NAMED_UNIT(*)
PLANE_ANGLE_UNIT()
SI_UNIT($,.RADIAN.)
);
#5662=(
NAMED_UNIT(*)
SI_UNIT($,.STERADIAN.)
SOLID_ANGLE_UNIT()
);
#5674=SHAPE_DEFINITION_REPRESENTATION(#5686,#5716);
#5686=PRODUCT_DEFINITION_SHAPE('',$,#5729);
#5716=SHAPE_REPRESENTATION('',(#3503),#5657);
#5717=PRODUCT_DEFINITION_CONTEXT('part definition',#5755,'design');
#5729=PRODUCT_DEFINITION('Socket Head Cap Screw M8 x 1.25 x 25',
'Socket Head Cap Screw M8 x 1.25 x 25',#5741,#5717);
#5741=PRODUCT_DEFINITION_FORMATION('',$,#5768);
#5755=APPLICATION_CONTEXT(
'Core Data for Automotive Mechanical Design Process');
#5756=PRODUCT_CONTEXT('part definition',#5755,'mechanical');
#5768=PRODUCT('Socket Head Cap Screw M8 x 1.25 x 25',
'Socket Head Cap Screw M8 x 1.25 x 25',$,(#5756));
#5770=PRESENTATION_STYLE_ASSIGNMENT((#5775));
#5775=SURFACE_STYLE_USAGE(.BOTH.,#5780);
#5780=SURFACE_SIDE_STYLE('',(#5785));
#5785=SURFACE_STYLE_FILL_AREA(#5790);
#5790=FILL_AREA_STYLE('Opaque(31,36,43)',(#5795));
#5795=FILL_AREA_STYLE_COLOUR('Opaque(31,36,43)',#5800);
#5800=COLOUR_RGB('Opaque(31,36,43)',0.12156862745098,0.141176470588235,
0.168627450980392);
ENDSEC;
END-ISO-10303-21;
